ISO-10303-21;
HEADER;
FILE_DESCRIPTION (('STEP AP214'),
    '1' );
FILE_NAME ('roller axis assy_r3.step',
    '2026-10-24T11:01:53',
    ( '' ),
    ( '' ),
    'SwSTEP 2.0',
    'SolidWorks 2026',
    '' );
FILE_SCHEMA (( 'AUTOMOTIVE_DESIGN' ));
ENDSEC;

DATA;
#12=CARTESIAN_POINT ( 'NONE',  ( -5.000000000000000000, -5.000000000000000000, 148.0000000000000284 ) ) ;
#17=LINE ( 'NONE', #599, #1287 ) ;
#55=DIRECTION ( 'NONE',  ( 1.734723475976806848E-16, -1.000000000000000000, -0.000000000000000000 ) ) ;
#56=CARTESIAN_POINT ( 'NONE',  ( 10.00000000000000000, 0.000000000000000000, 140.0000000000000000 ) ) ;
#103=DIRECTION ( 'NONE',  ( 0.000000000000000000, 0.000000000000000000, -1.000000000000000000 ) ) ;
#123=DIRECTION ( 'NONE',  ( 0.000000000000000000, -0.000000000000000000, 1.000000000000000000 ) ) ;
#132=ADVANCED_FACE ( 'NONE', ( #686, #1511 ), #6069, .T. ) ;
#141=ORIENTED_EDGE ( 'NONE', *, *, #4885, .F. ) ;
#147=VERTEX_POINT ( 'NONE', #2776 ) ;
#164=CIRCLE ( 'NONE', #2122, 10.00000000000000000 ) ;
#200=EDGE_CURVE ( 'NONE', #6574, #3690, #7176, .T. ) ;
#215=FACE_OUTER_BOUND ( 'NONE', #5011, .T. ) ;
#243=VERTEX_POINT ( 'NONE', #1034 ) ;
#284=ORIENTED_EDGE ( 'NONE', *, *, #8567, .F. ) ;
#336=DIRECTION ( 'NONE',  ( 1.000000000000000000, 0.000000000000000000, 0.000000000000000000 ) ) ;
#338=EDGE_CURVE ( 'NONE', #2469, #1525, #4337, .T. ) ;
#349=( LENGTH_UNIT ( ) NAMED_UNIT ( * ) SI_UNIT ( .MILLI., .METRE. ) );
#351=APPLICATION_CONTEXT ( 'automotive_design' ) ;
#355=DIRECTION ( 'NONE',  ( 1.000000000000000000, 0.000000000000000000, 0.000000000000000000 ) ) ;
#379=DIRECTION ( 'NONE',  ( -0.000000000000000000, -0.000000000000000000, 1.000000000000000000 ) ) ;
#404=FACE_OUTER_BOUND ( 'NONE', #903, .T. ) ;
#411=AXIS2_PLACEMENT_3D ( 'NONE', #7547, #5624, #7640 ) ;
#420=ORIENTED_EDGE ( 'NONE', *, *, #3116, .F. ) ;
#422=CARTESIAN_POINT ( 'NONE',  ( -5.000000000000000000, -5.000000000000000000, -71.99999999999998579 ) ) ;
#460=EDGE_LOOP ( 'NONE', ( #4338, #6382, #7676, #2437 ) ) ;
#464=DIRECTION ( 'NONE',  ( 0.000000000000000000, 0.000000000000000000, 1.000000000000000000 ) ) ;
#479=VERTEX_POINT ( 'NONE', #7117 ) ;
#482=ADVANCED_FACE ( 'NONE', ( #3818 ), #1820, .F. ) ;
#489=VERTEX_POINT ( 'NONE', #588 ) ;
#514=ORIENTED_EDGE ( 'NONE', *, *, #6408, .T. ) ;
#525=EDGE_CURVE ( 'NONE', #989, #7549, #930, .T. ) ;
#533=FACE_OUTER_BOUND ( 'NONE', #460, .T. ) ;
#543=DIRECTION ( 'NONE',  ( -1.734723475976806848E-16, 1.000000000000000000, 0.000000000000000000 ) ) ;
#546=AXIS2_PLACEMENT_3D ( 'NONE', #7851, #3806, #1061 ) ;
#549=CARTESIAN_POINT ( 'NONE',  ( 5.000000000000000000, -5.000000000000000000, 140.0000000000000000 ) ) ;
#569=CARTESIAN_POINT ( 'NONE',  ( 0.000000000000000000, 0.000000000000000000, 140.0000000000000000 ) ) ;
#588=CARTESIAN_POINT ( 'NONE',  ( 10.00000000000000000, 0.000000000000000000, -63.99999999999997158 ) ) ;
#594=AXIS2_PLACEMENT_3D ( 'NONE', #3123, #464, #5764 ) ;
#599=CARTESIAN_POINT ( 'NONE',  ( -5.000000000000000000, -5.000000000000000000, 140.0000000000000000 ) ) ;
#614=EDGE_LOOP ( 'NONE', ( #2947, #918 ) ) ;
#625=LINE ( 'NONE', #2721, #7491 ) ;
#636=LINE ( 'NONE', #12, #7410 ) ;
#642=SHAPE_DEFINITION_REPRESENTATION ( #4132, #7424 ) ;
#644=DIRECTION ( 'NONE',  ( 1.000000000000000000, 1.734723475976806848E-16, 0.000000000000000000 ) ) ;
#649=VECTOR ( 'NONE', #3687, 1000.000000000000000 ) ;
#651=STYLED_ITEM('',(#8678),#2244);
#665=( LENGTH_UNIT ( ) NAMED_UNIT ( * ) SI_UNIT ( .MILLI., .METRE. ) );
#684=ORIENTED_EDGE ( 'NONE', *, *, #4886, .F. ) ;
#686=FACE_BOUND ( 'NONE', #6675, .T. ) ;
#696=EDGE_LOOP ( 'NONE', ( #1832, #514, #6791, #6324 ) ) ;
#712=MECHANICAL_DESIGN_GEOMETRIC_PRESENTATION_REPRESENTATION('',(#6410),#7388);
#732=VERTEX_POINT ( 'NONE', #4102 ) ;
#760=CARTESIAN_POINT ( 'NONE',  ( -5.000000000000001776, 5.000000000000001776, 148.0000000000000284 ) ) ;
#799=CARTESIAN_POINT ( 'NONE',  ( -10.00000000000000000, 1.224646799147353256E-15, 120.0000000000000284 ) ) ;
#815=DIRECTION ( 'NONE',  ( -1.000000000000000000, 0.000000000000000000, -0.000000000000000000 ) ) ;
#820=DIRECTION ( 'NONE',  ( -0.000000000000000000, -0.000000000000000000, 1.000000000000000000 ) ) ;
#827=CARTESIAN_POINT ( 'NONE',  ( -5.000000000000000000, -5.000000000000000000, -71.99999999999998579 ) ) ;
#842=CARTESIAN_POINT ( 'NONE',  ( 0.000000000000000000, 0.000000000000000000, 140.0000000000000000 ) ) ;
#890=CARTESIAN_POINT ( 'NONE',  ( 0.000000000000000000, 0.000000000000000000, -43.99999999999997158 ) ) ;
#893=ORIENTED_EDGE ( 'NONE', *, *, #8129, .F. ) ;
#903=EDGE_LOOP ( 'NONE', ( #3099, #6280, #8023, #6203 ) ) ;
#918=ORIENTED_EDGE ( 'NONE', *, *, #4465, .T. ) ;
#930=CIRCLE ( 'NONE', #5649, 10.00000000000000000 ) ;
#945=LINE ( 'NONE', #6810, #2868 ) ;
#954=LINE ( 'NONE', #6033, #1288 ) ;
#959=VECTOR ( 'NONE', #4708, 1000.000000000000000 ) ;
#963=ORIENTED_EDGE ( 'NONE', *, *, #338, .T. ) ;
#973=CARTESIAN_POINT ( 'NONE',  ( -10.00000000000000000, 1.224646799147353256E-15, -43.99999999999997158 ) ) ;
#974=AXIS2_PLACEMENT_3D ( 'NONE', #6798, #8163, #2152 ) ;
#977=FACE_OUTER_BOUND ( 'NONE', #5652, .T. ) ;
#989=VERTEX_POINT ( 'NONE', #3745 ) ;
#1008=FACE_BOUND ( 'NONE', #1463, .T. ) ;
#1020=DIRECTION ( 'NONE',  ( -0.000000000000000000, -0.000000000000000000, 1.000000000000000000 ) ) ;
#1034=CARTESIAN_POINT ( 'NONE',  ( -5.000000000000001776, 5.000000000000001776, 140.0000000000000000 ) ) ;
#1051=DIRECTION ( 'NONE',  ( 0.000000000000000000, 0.000000000000000000, 1.000000000000000000 ) ) ;
#1061=DIRECTION ( 'NONE',  ( 1.000000000000000000, 0.000000000000000000, 0.000000000000000000 ) ) ;
#1065=AXIS2_PLACEMENT_3D ( 'NONE', #2120, #1381, #4039 ) ;
#1097=DIRECTION ( 'NONE',  ( -1.000000000000000000, 0.000000000000000000, -0.000000000000000000 ) ) ;
#1154=FACE_OUTER_BOUND ( 'NONE', #3518, .T. ) ;
#1175=ORIENTED_EDGE ( 'NONE', *, *, #7440, .F. ) ;
#1183=CARTESIAN_POINT ( 'NONE',  ( 0.000000000000000000, 0.000000000000000000, 140.0000000000000000 ) ) ;
#1242=DIRECTION ( 'NONE',  ( 0.000000000000000000, 1.000000000000000000, 0.000000000000000000 ) ) ;
#1243=VECTOR ( 'NONE', #4493, 1000.000000000000000 ) ;
#1266=EDGE_LOOP ( 'NONE', ( #5909, #963, #5140, #6871 ) ) ;
#1275=DIRECTION ( 'NONE',  ( 0.000000000000000000, 0.000000000000000000, 1.000000000000000000 ) ) ;
#1287=VECTOR ( 'NONE', #2042, 1000.000000000000000 ) ;
#1288=VECTOR ( 'NONE', #820, 1000.000000000000000 ) ;
#1309=AXIS2_PLACEMENT_3D ( 'NONE', #5172, #1051, #4439 ) ;
#1380=EDGE_CURVE ( 'NONE', #2207, #5505, #6471, .T. ) ;
#1381=DIRECTION ( 'NONE',  ( 0.000000000000000000, 0.000000000000000000, 1.000000000000000000 ) ) ;
#1424=AXIS2_PLACEMENT_3D ( 'NONE', #3135, #8322, #6436 ) ;
#1437=VECTOR ( 'NONE', #5283, 1000.000000000000000 ) ;
#1448=VECTOR ( 'NONE', #1962, 1000.000000000000000 ) ;
#1463=EDGE_LOOP ( 'NONE', ( #5434, #8450, #5094, #893 ) ) ;
#1478=CLOSED_SHELL ( 'NONE', ( #4062, #4552, #4311, #4235, #4388, #4568, #5994, #3402, #6076, #8173, #132, #3939, #6835, #4648, #3541, #482, #2530, #6537, #2671, #3502 ) ) ;
#1501=VERTEX_POINT ( 'NONE', #549 ) ;
#1511=FACE_OUTER_BOUND ( 'NONE', #5220, .T. ) ;
#1518=AXIS2_PLACEMENT_3D ( 'NONE', #3204, #5235, #336 ) ;
#1525=VERTEX_POINT ( 'NONE', #7247 ) ;
#1537=DIRECTION ( 'NONE',  ( 0.000000000000000000, 0.000000000000000000, 1.000000000000000000 ) ) ;
#1555=CARTESIAN_POINT ( 'NONE',  ( 0.000000000000000000, 0.000000000000000000, 148.0000000000000284 ) ) ;
#1603=ORIENTED_EDGE ( 'NONE', *, *, #1380, .T. ) ;
#1651=LINE ( 'NONE', #422, #5314 ) ;
#1653=EDGE_CURVE ( 'NONE', #147, #5734, #945, .T. ) ;
#1667=DIRECTION ( 'NONE',  ( 0.000000000000000000, 0.000000000000000000, -1.000000000000000000 ) ) ;
#1671=AXIS2_PLACEMENT_3D ( 'NONE', #7190, #1806, #2547 ) ;
#1711=ORIENTED_EDGE ( 'NONE', *, *, #3167, .F. ) ;
#1712=LINE ( 'NONE', #5660, #6937 ) ;
#1720=DIRECTION ( 'NONE',  ( 1.000000000000000000, 0.000000000000000000, 0.000000000000000000 ) ) ;
#1724=ORIENTED_EDGE ( 'NONE', *, *, #6796, .F. ) ;
#1747=VERTEX_POINT ( 'NONE', #6941 ) ;
#1749=DIRECTION ( 'NONE',  ( -1.000000000000000000, 0.000000000000000000, 0.000000000000000000 ) ) ;
#1761=CYLINDRICAL_SURFACE ( 'NONE', #7798, 10.00000000000000000 ) ;
#1793=ORIENTED_EDGE ( 'NONE', *, *, #525, .T. ) ;
#1806=DIRECTION ( 'NONE',  ( -1.734723475976806848E-16, -1.000000000000000000, 0.000000000000000000 ) ) ;
#1811=DIRECTION ( 'NONE',  ( -0.000000000000000000, -0.000000000000000000, 1.000000000000000000 ) ) ;
#1820=PLANE ( 'NONE',  #8582 ) ;
#1832=ORIENTED_EDGE ( 'NONE', *, *, #2960, .T. ) ;
#1846=AXIS2_PLACEMENT_3D ( 'NONE', #3961, #644, #5900 ) ;
#1851=CARTESIAN_POINT ( 'NONE',  ( 5.000000000000000000, 5.000000000000000000, 148.0000000000000284 ) ) ;
#1853=LINE ( 'NONE', #3485, #5109 ) ;
#1927=ORIENTED_EDGE ( 'NONE', *, *, #4704, .F. ) ;
#1930=DIRECTION ( 'NONE',  ( 0.000000000000000000, 0.000000000000000000, 1.000000000000000000 ) ) ;
#1938=CARTESIAN_POINT ( 'NONE',  ( 5.000000000000000000, -5.000000000000000000, 148.0000000000000284 ) ) ;
#1946=ORIENTED_EDGE ( 'NONE', *, *, #5666, .T. ) ;
#1962=DIRECTION ( 'NONE',  ( -1.000000000000000000, 0.000000000000000000, 0.000000000000000000 ) ) ;
#1966=ORIENTED_EDGE ( 'NONE', *, *, #6635, .F. ) ;
#1981=LINE ( 'NONE', #6757, #3605 ) ;
#1984=ORIENTED_EDGE ( 'NONE', *, *, #6886, .F. ) ;
#1996=CIRCLE ( 'NONE', #3523, 20.00000000000000000 ) ;
#2027=DIRECTION ( 'NONE',  ( 0.000000000000000000, 0.000000000000000000, 1.000000000000000000 ) ) ;
#2033=ORIENTED_EDGE ( 'NONE', *, *, #3534, .F. ) ;
#2042=DIRECTION ( 'NONE',  ( 1.000000000000000000, 0.000000000000000000, 0.000000000000000000 ) ) ;
#2045=DIRECTION ( 'NONE',  ( 0.000000000000000000, 0.000000000000000000, -1.000000000000000000 ) ) ;
#2063=CARTESIAN_POINT ( 'NONE',  ( 5.000000000000000000, -5.000000000000000000, 148.0000000000000284 ) ) ;
#2120=CARTESIAN_POINT ( 'NONE',  ( 0.000000000000000000, 0.000000000000000000, 120.0000000000000284 ) ) ;
#2122=AXIS2_PLACEMENT_3D ( 'NONE', #4845, #1537, #4184 ) ;
#2135=CARTESIAN_POINT ( 'NONE',  ( -5.000000000000000000, -5.000000000000000000, -63.99999999999997158 ) ) ;
#2150=DIRECTION ( 'NONE',  ( -1.000000000000000000, 0.000000000000000000, 0.000000000000000000 ) ) ;
#2152=DIRECTION ( 'NONE',  ( 1.000000000000000000, 0.000000000000000000, 0.000000000000000000 ) ) ;
#2189=DIRECTION ( 'NONE',  ( 0.000000000000000000, 1.000000000000000000, 0.000000000000000000 ) ) ;
#2207=VERTEX_POINT ( 'NONE', #2135 ) ;
#2244=MANIFOLD_SOLID_BREP ( 'Boss-Extrude4', #1478 ) ;
#2246=COLOUR_RGB ( '',0.8941176470588234615, 0.8941176470588234615, 0.8941176470588234615 ) ;
#2251=APPLICATION_CONTEXT ( 'automotive_design' ) ;
#2252=CARTESIAN_POINT ( 'NONE',  ( -5.000000000000001776, 5.000000000000001776, 148.0000000000000284 ) ) ;
#2270=VECTOR ( 'NONE', #1930, 1000.000000000000000 ) ;
#2271=EDGE_CURVE ( 'NONE', #6071, #7348, #1853, .T. ) ;
#2281=PLANE ( 'NONE',  #4149 ) ;
#2285=CARTESIAN_POINT ( 'NONE',  ( 0.000000000000000000, 0.000000000000000000, -43.99999999999997158 ) ) ;
#2292=AXIS2_PLACEMENT_3D ( 'NONE', #1938, #5922, #2512 ) ;
#2294=ORIENTED_EDGE ( 'NONE', *, *, #7291, .T. ) ;
#2301=AXIS2_PLACEMENT_3D ( 'NONE', #8518, #1242, #6546 ) ;
#2305=ORIENTED_EDGE ( 'NONE', *, *, #7524, .F. ) ;
#2307=CARTESIAN_POINT ( 'NONE',  ( -5.000000000000001776, 5.000000000000001776, -71.99999999999998579 ) ) ;
#2309=ORIENTED_EDGE ( 'NONE', *, *, #2271, .F. ) ;
#2335=CARTESIAN_POINT ( 'NONE',  ( 0.000000000000000000, 0.000000000000000000, -71.99999999999998579 ) ) ;
#2376=AXIS2_PLACEMENT_3D ( 'NONE', #4715, #1275, #6584 ) ;
#2425=CIRCLE ( 'NONE', #7129, 10.00000000000000000 ) ;
#2435=EDGE_CURVE ( 'NONE', #3488, #2469, #8028, .T. ) ;
#2437=ORIENTED_EDGE ( 'NONE', *, *, #5827, .F. ) ;
#2452=CARTESIAN_POINT ( 'NONE',  ( -5.000000000000001776, 5.000000000000001776, -63.99999999999997158 ) ) ;
#2469=VERTEX_POINT ( 'NONE', #3494 ) ;
#2491=FACE_BOUND ( 'NONE', #4114, .T. ) ;
#2494=ORIENTED_EDGE ( 'NONE', *, *, #5666, .F. ) ;
#2512=DIRECTION ( 'NONE',  ( 0.000000000000000000, 0.000000000000000000, 1.000000000000000000 ) ) ;
#2527=DIRECTION ( 'NONE',  ( 0.000000000000000000, 0.000000000000000000, 1.000000000000000000 ) ) ;
#2530=ADVANCED_FACE ( 'NONE', ( #215 ), #2281, .F. ) ;
#2547=DIRECTION ( 'NONE',  ( 1.000000000000000000, -1.734723475976806848E-16, 0.000000000000000000 ) ) ;
#2554=CIRCLE ( 'NONE', #3799, 10.00000000000000000 ) ;
#2612=DIRECTION ( 'NONE',  ( 0.000000000000000000, 0.000000000000000000, -1.000000000000000000 ) ) ;
#2651=ORIENTED_EDGE ( 'NONE', *, *, #4741, .F. ) ;
#2659=PRESENTATION_STYLE_ASSIGNMENT (( #8544 ) ) ;
#2671=ADVANCED_FACE ( 'NONE', ( #7141, #1008 ), #5093, .F. ) ;
#2682=DIRECTION ( 'NONE',  ( -1.734723475976806848E-16, -1.000000000000000000, 0.000000000000000000 ) ) ;
#2694=DIRECTION ( 'NONE',  ( 0.000000000000000000, 0.000000000000000000, 1.000000000000000000 ) ) ;
#2721=CARTESIAN_POINT ( 'NONE',  ( 5.000000000000000000, 5.000000000000000000, -63.99999999999997158 ) ) ;
#2776=CARTESIAN_POINT ( 'NONE',  ( -5.000000000000000000, -5.000000000000000000, 148.0000000000000284 ) ) ;
#2779=EDGE_LOOP ( 'NONE', ( #7267, #8266, #284, #8531 ) ) ;
#2780=ORIENTED_EDGE ( 'NONE', *, *, #4885, .T. ) ;
#2787=( NAMED_UNIT ( * ) PLANE_ANGLE_UNIT ( ) SI_UNIT ( $, .RADIAN. ) );
#2804=ORIENTED_EDGE ( 'NONE', *, *, #5409, .F. ) ;
#2815=CARTESIAN_POINT ( 'NONE',  ( 10.00000000000000000, 0.000000000000000000, -43.99999999999997158 ) ) ;
#2818=PLANE ( 'NONE',  #5169 ) ;
#2831=DIRECTION ( 'NONE',  ( 0.000000000000000000, -1.000000000000000000, 0.000000000000000000 ) ) ;
#2868=VECTOR ( 'NONE', #4079, 1000.000000000000000 ) ;
#2894=CARTESIAN_POINT ( 'NONE',  ( -5.000000000000000000, -5.000000000000000000, 140.0000000000000000 ) ) ;
#2947=ORIENTED_EDGE ( 'NONE', *, *, #3116, .T. ) ;
#2948=PRODUCT_DEFINITION_FORMATION_WITH_SPECIFIED_SOURCE ( 'ANY', '', #8104, .NOT_KNOWN. ) ;
#2951=VECTOR ( 'NONE', #5667, 1000.000000000000000 ) ;
#2954=CARTESIAN_POINT ( 'NONE',  ( 0.000000000000000000, 0.000000000000000000, -63.99999999999997158 ) ) ;
#2960=EDGE_CURVE ( 'NONE', #732, #3015, #4786, .T. ) ;
#2976=DIRECTION ( 'NONE',  ( 0.000000000000000000, 0.000000000000000000, -1.000000000000000000 ) ) ;
#2985=ORIENTED_EDGE ( 'NONE', *, *, #200, .F. ) ;
#3015=VERTEX_POINT ( 'NONE', #7900 ) ;
#3055=CYLINDRICAL_SURFACE ( 'NONE', #1309, 20.00000000000000000 ) ;
#3089=PLANE ( 'NONE',  #1424 ) ;
#3092=EDGE_LOOP ( 'NONE', ( #1711, #6658, #6786, #5840 ) ) ;
#3099=ORIENTED_EDGE ( 'NONE', *, *, #8129, .T. ) ;
#3113=VECTOR ( 'NONE', #3560, 1000.000000000000000 ) ;
#3116=EDGE_CURVE ( 'NONE', #1747, #6101, #5022, .T. ) ;
#3118=VECTOR ( 'NONE', #55, 1000.000000000000000 ) ;
#3123=CARTESIAN_POINT ( 'NONE',  ( 0.000000000000000000, 0.000000000000000000, 0.000000000000000000 ) ) ;
#3124=DIRECTION ( 'NONE',  ( 1.000000000000000000, 1.734723475976806848E-16, -0.000000000000000000 ) ) ;
#3135=CARTESIAN_POINT ( 'NONE',  ( 0.000000000000000000, 0.000000000000000000, -63.99999999999997158 ) ) ;
#3147=ORIENTED_EDGE ( 'NONE', *, *, #7407, .T. ) ;
#3159=EDGE_CURVE ( 'NONE', #6262, #489, #5402, .T. ) ;
#3167=EDGE_CURVE ( 'NONE', #7751, #6101, #1981, .T. ) ;
#3204=CARTESIAN_POINT ( 'NONE',  ( 0.000000000000000000, 0.000000000000000000, 120.0000000000000142 ) ) ;
#3216=DIRECTION ( 'NONE',  ( 1.000000000000000000, 0.000000000000000000, 0.000000000000000000 ) ) ;
#3217=ORIENTED_EDGE ( 'NONE', *, *, #5827, .T. ) ;
#3229=SURFACE_SIDE_STYLE ('',( #8586 ) ) ;
#3244=VECTOR ( 'NONE', #379, 1000.000000000000000 ) ;
#3250=ORIENTED_EDGE ( 'NONE', *, *, #200, .T. ) ;
#3252=LINE ( 'NONE', #4509, #1437 ) ;
#3261=ORIENTED_EDGE ( 'NONE', *, *, #7524, .T. ) ;
#3282=EDGE_CURVE ( 'NONE', #479, #7567, #625, .T. ) ;
#3300=EDGE_CURVE ( 'NONE', #4379, #7751, #6090, .T. ) ;
#3338=LINE ( 'NONE', #4635, #7550 ) ;
#3402=ADVANCED_FACE ( 'NONE', ( #977 ), #3588, .F. ) ;
#3441=VERTEX_POINT ( 'NONE', #4412 ) ;
#3471=CARTESIAN_POINT ( 'NONE',  ( 5.000000000000000000, -5.000000000000000000, -71.99999999999998579 ) ) ;
#3485=CARTESIAN_POINT ( 'NONE',  ( 5.000000000000000000, 5.000000000000000000, -71.99999999999998579 ) ) ;
#3488=VERTEX_POINT ( 'NONE', #7061 ) ;
#3494=CARTESIAN_POINT ( 'NONE',  ( 5.000000000000000000, 5.000000000000000000, 148.0000000000000284 ) ) ;
#3502=ADVANCED_FACE ( 'NONE', ( #5753 ), #5104, .T. ) ;
#3518=EDGE_LOOP ( 'NONE', ( #3147, #2033, #6113, #4203 ) ) ;
#3523=AXIS2_PLACEMENT_3D ( 'NONE', #6517, #2694, #7872 ) ;
#3534=EDGE_CURVE ( 'NONE', #2469, #3441, #6364, .T. ) ;
#3541=ADVANCED_FACE ( 'NONE', ( #404 ), #7769, .F. ) ;
#3555=DIRECTION ( 'NONE',  ( -1.000000000000000000, 0.000000000000000000, 0.000000000000000000 ) ) ;
#3560=DIRECTION ( 'NONE',  ( -0.000000000000000000, -0.000000000000000000, -1.000000000000000000 ) ) ;
#3574=LINE ( 'NONE', #6223, #6311 ) ;
#3579=CARTESIAN_POINT ( 'NONE',  ( -5.000000000000000000, -5.000000000000000000, 148.0000000000000284 ) ) ;
#3588=PLANE ( 'NONE',  #411 ) ;
#3601=LINE ( 'NONE', #7812, #5445 ) ;
#3605=VECTOR ( 'NONE', #2027, 1000.000000000000000 ) ;
#3646=CARTESIAN_POINT ( 'NONE',  ( -10.00000000000000000, 1.224646799147353256E-15, -63.99999999999997158 ) ) ;
#3647=VECTOR ( 'NONE', #8122, 1000.000000000000000 ) ;
#3674=CYLINDRICAL_SURFACE ( 'NONE', #974, 10.00000000000000000 ) ;
#3684=ORIENTED_EDGE ( 'NONE', *, *, #7315, .F. ) ;
#3687=DIRECTION ( 'NONE',  ( -1.000000000000000000, 1.734723475976806848E-16, -0.000000000000000000 ) ) ;
#3689=EDGE_CURVE ( 'NONE', #147, #3488, #7363, .T. ) ;
#3690=VERTEX_POINT ( 'NONE', #799 ) ;
#3703=DIRECTION ( 'NONE',  ( -1.000000000000000000, 0.000000000000000000, 0.000000000000000000 ) ) ;
#3706=AXIS2_PLACEMENT_3D ( 'NONE', #4121, #103, #815 ) ;
#3745=CARTESIAN_POINT ( 'NONE',  ( -10.00000000000000000, 1.224646799147353256E-15, 140.0000000000000000 ) ) ;
#3747=ORIENTED_EDGE ( 'NONE', *, *, #3832, .F. ) ;
#3780=PRODUCT_DEFINITION ( 'UNKNOWN', '', #2948, #3954 ) ;
#3796=EDGE_LOOP ( 'NONE', ( #1603, #2651, #4939, #2294 ) ) ;
#3799=AXIS2_PLACEMENT_3D ( 'NONE', #5696, #5780, #1749 ) ;
#3806=DIRECTION ( 'NONE',  ( -0.000000000000000000, -0.000000000000000000, 1.000000000000000000 ) ) ;
#3811=DIRECTION ( 'NONE',  ( -0.000000000000000000, -0.000000000000000000, 1.000000000000000000 ) ) ;
#3818=FACE_OUTER_BOUND ( 'NONE', #6390, .T. ) ;
#3826=ORIENTED_EDGE ( 'NONE', *, *, #7991, .T. ) ;
#3832=EDGE_CURVE ( 'NONE', #6574, #7549, #1712, .T. ) ;
#3876=CARTESIAN_POINT ( 'NONE',  ( 0.000000000000000000, 0.000000000000000000, -43.99999999999997158 ) ) ;
#3915=DIRECTION ( 'NONE',  ( -1.000000000000000000, 0.000000000000000000, 0.000000000000000000 ) ) ;
#3939=ADVANCED_FACE ( 'NONE', ( #4064, #5925 ), #6708, .T. ) ;
#3954=PRODUCT_DEFINITION_CONTEXT ( 'detailed design', #2251, 'design' ) ;
#3961=CARTESIAN_POINT ( 'NONE',  ( -5.000000000000000000, -5.000000000000000000, -71.99999999999998579 ) ) ;
#3969=ORIENTED_EDGE ( 'NONE', *, *, #1653, .F. ) ;
#3972=CARTESIAN_POINT ( 'NONE',  ( 20.00000000000000000, 0.000000000000000000, -120.5685424949237898 ) ) ;
#4031=AXIS2_PLACEMENT_3D ( 'NONE', #7019, #5187, #355 ) ;
#4039=DIRECTION ( 'NONE',  ( 1.000000000000000000, 0.000000000000000000, 0.000000000000000000 ) ) ;
#4062=ADVANCED_FACE ( 'NONE', ( #8297 ), #3674, .T. ) ;
#4064=FACE_BOUND ( 'NONE', #6863, .T. ) ;
#4079=DIRECTION ( 'NONE',  ( -0.000000000000000000, -0.000000000000000000, -1.000000000000000000 ) ) ;
#4095=ORIENTED_EDGE ( 'NONE', *, *, #3159, .T. ) ;
#4102=CARTESIAN_POINT ( 'NONE',  ( -5.000000000000000000, -5.000000000000000000, -71.99999999999998579 ) ) ;
#4114=EDGE_LOOP ( 'NONE', ( #7237, #4296, #5435, #1724 ) ) ;
#4121=CARTESIAN_POINT ( 'NONE',  ( 0.000000000000000000, 0.000000000000000000, -43.99999999999997158 ) ) ;
#4123=DIRECTION ( 'NONE',  ( -1.000000000000000000, 0.000000000000000000, -0.000000000000000000 ) ) ;
#4132=PRODUCT_DEFINITION_SHAPE ( 'NONE', 'NONE',  #3780 ) ;
#4145=LINE ( 'NONE', #760, #3647 ) ;
#4149=AXIS2_PLACEMENT_3D ( 'NONE', #3579, #2189, #123 ) ;
#4155=EDGE_LOOP ( 'NONE', ( #8128, #2305, #4882, #6504 ) ) ;
#4165=ORIENTED_EDGE ( 'NONE', *, *, #6239, .T. ) ;
#4184=DIRECTION ( 'NONE',  ( 1.000000000000000000, 0.000000000000000000, 0.000000000000000000 ) ) ;
#4199=CIRCLE ( 'NONE', #6560, 10.00000000000000000 ) ;
#4203=ORIENTED_EDGE ( 'NONE', *, *, #7177, .T. ) ;
#4227=VECTOR ( 'NONE', #7735, 1000.000000000000000 ) ;
#4235=ADVANCED_FACE ( 'NONE', ( #8468 ), #5146, .T. ) ;
#4236=LINE ( 'NONE', #7726, #2951 ) ;
#4262=ORIENTED_EDGE ( 'NONE', *, *, #6635, .T. ) ;
#4289=AXIS2_PLACEMENT_3D ( 'NONE', #1183, #1667, #1097 ) ;
#4296=ORIENTED_EDGE ( 'NONE', *, *, #6919, .F. ) ;
#4311=ADVANCED_FACE ( 'NONE', ( #533 ), #1761, .T. ) ;
#4323=DIRECTION ( 'NONE',  ( -1.000000000000000000, 0.000000000000000000, 0.000000000000000000 ) ) ;
#4337=LINE ( 'NONE', #2252, #649 ) ;
#4338=ORIENTED_EDGE ( 'NONE', *, *, #3159, .F. ) ;
#4341=LINE ( 'NONE', #3646, #3244 ) ;
#4379=VERTEX_POINT ( 'NONE', #5732 ) ;
#4388=ADVANCED_FACE ( 'NONE', ( #2491, #5129 ), #3089, .T. ) ;
#4400=CARTESIAN_POINT ( 'NONE',  ( -5.000000000000001776, 5.000000000000001776, -63.99999999999997158 ) ) ;
#4412=CARTESIAN_POINT ( 'NONE',  ( 5.000000000000000000, 5.000000000000000000, 140.0000000000000000 ) ) ;
#4439=DIRECTION ( 'NONE',  ( 1.000000000000000000, 0.000000000000000000, 0.000000000000000000 ) ) ;
#4462=CARTESIAN_POINT ( 'NONE',  ( -5.000000000000000000, -5.000000000000000000, 148.0000000000000284 ) ) ;
#4465=EDGE_CURVE ( 'NONE', #6101, #1747, #1996, .T. ) ;
#4475=ORIENTED_EDGE ( 'NONE', *, *, #1653, .T. ) ;
#4485=ORIENTED_EDGE ( 'NONE', *, *, #4994, .T. ) ;
#4493=DIRECTION ( 'NONE',  ( -0.000000000000000000, -0.000000000000000000, -1.000000000000000000 ) ) ;
#4509=CARTESIAN_POINT ( 'NONE',  ( 5.000000000000000000, -5.000000000000000000, 140.0000000000000000 ) ) ;
#4518=FACE_OUTER_BOUND ( 'NONE', #3092, .T. ) ;
#4552=ADVANCED_FACE ( 'NONE', ( #8490 ), #6642, .T. ) ;
#4568=ADVANCED_FACE ( 'NONE', ( #4596 ), #5855, .F. ) ;
#4577=CARTESIAN_POINT ( 'NONE',  ( 10.00000000000000000, 0.000000000000000000, 120.0000000000000284 ) ) ;
#4596=FACE_OUTER_BOUND ( 'NONE', #3796, .T. ) ;
#4634=PLANE ( 'NONE',  #2301 ) ;
#4635=CARTESIAN_POINT ( 'NONE',  ( 5.000000000000000000, 5.000000000000000000, -71.99999999999998579 ) ) ;
#4648=ADVANCED_FACE ( 'NONE', ( #8097 ), #2818, .F. ) ;
#4704=EDGE_CURVE ( 'NONE', #7348, #7567, #3601, .T. ) ;
#4708=DIRECTION ( 'NONE',  ( 0.000000000000000000, 1.000000000000000000, 0.000000000000000000 ) ) ;
#4715=CARTESIAN_POINT ( 'NONE',  ( 0.000000000000000000, 0.000000000000000000, 120.0000000000000142 ) ) ;
#4741=EDGE_CURVE ( 'NONE', #3015, #5505, #8269, .T. ) ;
#4786=LINE ( 'NONE', #827, #5539 ) ;
#4817=LINE ( 'NONE', #3471, #8397 ) ;
#4821=EDGE_LOOP ( 'NONE', ( #3250, #4262, #1793, #3747 ) ) ;
#4845=CARTESIAN_POINT ( 'NONE',  ( 0.000000000000000000, 0.000000000000000000, 120.0000000000000284 ) ) ;
#4851=AXIS2_PLACEMENT_3D ( 'NONE', #890, #1020, #4323 ) ;
#4882=ORIENTED_EDGE ( 'NONE', *, *, #6408, .F. ) ;
#4885=EDGE_CURVE ( 'NONE', #7549, #989, #4199, .T. ) ;
#4886=EDGE_CURVE ( 'NONE', #8169, #8541, #8519, .T. ) ;
#4908=CARTESIAN_POINT ( 'NONE',  ( -5.000000000000000000, -5.000000000000000000, 140.0000000000000000 ) ) ;
#4939=ORIENTED_EDGE ( 'NONE', *, *, #2960, .F. ) ;
#4943=ORIENTED_EDGE ( 'NONE', *, *, #7177, .F. ) ;
#4982=ORIENTED_EDGE ( 'NONE', *, *, #3167, .T. ) ;
#4994=EDGE_CURVE ( 'NONE', #3690, #6574, #164, .T. ) ;
#5010=DIRECTION ( 'NONE',  ( -0.000000000000000000, -0.000000000000000000, 1.000000000000000000 ) ) ;
#5011=EDGE_LOOP ( 'NONE', ( #5996, #4943, #7715, #4475 ) ) ;
#5022=CIRCLE ( 'NONE', #1518, 20.00000000000000000 ) ;
#5033=AXIS2_PLACEMENT_3D ( 'NONE', #7211, #2527, #3216 ) ;
#5065=CARTESIAN_POINT ( 'NONE',  ( -20.00000000000000000, 2.449293598294706513E-15, -43.99999999999997158 ) ) ;
#5066=UNCERTAINTY_MEASURE_WITH_UNIT (LENGTH_MEASURE( 1.000000000000000082E-05 ), #5349, 'distance_accuracy_value', 'NONE');
#5093=PLANE ( 'NONE',  #4289 ) ;
#5094=ORIENTED_EDGE ( 'NONE', *, *, #6239, .F. ) ;
#5097=MECHANICAL_DESIGN_GEOMETRIC_PRESENTATION_REPRESENTATION('',(#651),#6904);
#5104=CYLINDRICAL_SURFACE ( 'NONE', #546, 10.00000000000000000 ) ;
#5109=VECTOR ( 'NONE', #2831, 1000.000000000000000 ) ;
#5129=FACE_OUTER_BOUND ( 'NONE', #6817, .T. ) ;
#5140=ORIENTED_EDGE ( 'NONE', *, *, #7440, .T. ) ;
#5146=CYLINDRICAL_SURFACE ( 'NONE', #4031, 10.00000000000000000 ) ;
#5169=AXIS2_PLACEMENT_3D ( 'NONE', #1555, #2045, #4123 ) ;
#5170=ORIENTED_EDGE ( 'NONE', *, *, #3300, .T. ) ;
#5172=CARTESIAN_POINT ( 'NONE',  ( 0.000000000000000000, 0.000000000000000000, -120.5685424949237898 ) ) ;
#5181=EDGE_CURVE ( 'NONE', #4379, #1747, #6569, .T. ) ;
#5187=DIRECTION ( 'NONE',  ( -0.000000000000000000, -0.000000000000000000, 1.000000000000000000 ) ) ;
#5203=DIRECTION ( 'NONE',  ( 1.734723475976806848E-16, -1.000000000000000000, -0.000000000000000000 ) ) ;
#5214=CARTESIAN_POINT ( 'NONE',  ( 5.000000000000000000, -5.000000000000000000, -63.99999999999997158 ) ) ;
#5220=EDGE_LOOP ( 'NONE', ( #6549, #1984 ) ) ;
#5235=DIRECTION ( 'NONE',  ( 0.000000000000000000, 0.000000000000000000, 1.000000000000000000 ) ) ;
#5283=DIRECTION ( 'NONE',  ( 0.000000000000000000, 1.000000000000000000, 0.000000000000000000 ) ) ;
#5295=LINE ( 'NONE', #5214, #1448 ) ;
#5314=VECTOR ( 'NONE', #6428, 1000.000000000000000 ) ;
#5349=( LENGTH_UNIT ( ) NAMED_UNIT ( * ) SI_UNIT ( .MILLI., .METRE. ) );
#5402=CIRCLE ( 'NONE', #5686, 10.00000000000000000 ) ;
#5409=EDGE_CURVE ( 'NONE', #489, #6262, #2554, .T. ) ;
#5413=LINE ( 'NONE', #2894, #3118 ) ;
#5418=EDGE_LOOP ( 'NONE', ( #3684, #2804, #3217, #1946 ) ) ;
#5431=( NAMED_UNIT ( * ) SI_UNIT ( $, .STERADIAN. ) SOLID_ANGLE_UNIT ( ) );
#5434=ORIENTED_EDGE ( 'NONE', *, *, #7407, .F. ) ;
#5435=ORIENTED_EDGE ( 'NONE', *, *, #3282, .F. ) ;
#5444=DIRECTION ( 'NONE',  ( 0.000000000000000000, 0.000000000000000000, -1.000000000000000000 ) ) ;
#5445=VECTOR ( 'NONE', #1811, 1000.000000000000000 ) ;
#5453=EDGE_LOOP ( 'NONE', ( #141, #8214 ) ) ;
#5505=VERTEX_POINT ( 'NONE', #2452 ) ;
#5518=DIRECTION ( 'NONE',  ( -1.734723475976806848E-16, 1.000000000000000000, 0.000000000000000000 ) ) ;
#5539=VECTOR ( 'NONE', #5518, 1000.000000000000000 ) ;
#5557=LINE ( 'NONE', #7522, #3113 ) ;
#5573=FACE_OUTER_BOUND ( 'NONE', #696, .T. ) ;
#5624=DIRECTION ( 'NONE',  ( -1.000000000000000000, 0.000000000000000000, -0.000000000000000000 ) ) ;
#5631=LINE ( 'NONE', #5715, #4227 ) ;
#5649=AXIS2_PLACEMENT_3D ( 'NONE', #569, #7808, #7059 ) ;
#5652=EDGE_LOOP ( 'NONE', ( #8151, #1927, #2309, #3261 ) ) ;
#5660=CARTESIAN_POINT ( 'NONE',  ( 10.00000000000000000, 0.000000000000000000, -63.99999999999997158 ) ) ;
#5661=( NAMED_UNIT ( * ) SI_UNIT ( $, .STERADIAN. ) SOLID_ANGLE_UNIT ( ) );
#5666=EDGE_CURVE ( 'NONE', #8541, #8169, #2425, .T. ) ;
#5667=DIRECTION ( 'NONE',  ( -1.000000000000000000, 1.734723475976806848E-16, -0.000000000000000000 ) ) ;
#5686=AXIS2_PLACEMENT_3D ( 'NONE', #2954, #8278, #6952 ) ;
#5696=CARTESIAN_POINT ( 'NONE',  ( 0.000000000000000000, 0.000000000000000000, -63.99999999999997158 ) ) ;
#5715=CARTESIAN_POINT ( 'NONE',  ( -5.000000000000001776, 5.000000000000001776, -71.99999999999998579 ) ) ;
#5732=CARTESIAN_POINT ( 'NONE',  ( 20.00000000000000000, 0.000000000000000000, -43.99999999999997158 ) ) ;
#5734=VERTEX_POINT ( 'NONE', #4908 ) ;
#5753=FACE_OUTER_BOUND ( 'NONE', #8333, .T. ) ;
#5759=UNCERTAINTY_MEASURE_WITH_UNIT (LENGTH_MEASURE( 1.000000000000000082E-05 ), #349, 'distance_accuracy_value', 'NONE');
#5764=DIRECTION ( 'NONE',  ( 1.000000000000000000, 0.000000000000000000, 0.000000000000000000 ) ) ;
#5773=DIRECTION ( 'NONE',  ( -1.734723475976806848E-16, 1.000000000000000000, 0.000000000000000000 ) ) ;
#5780=DIRECTION ( 'NONE',  ( 0.000000000000000000, 0.000000000000000000, -1.000000000000000000 ) ) ;
#5827=EDGE_CURVE ( 'NONE', #489, #8541, #954, .T. ) ;
#5840=ORIENTED_EDGE ( 'NONE', *, *, #4465, .F. ) ;
#5845=FACE_OUTER_BOUND ( 'NONE', #2779, .T. ) ;
#5855=PLANE ( 'NONE',  #1846 ) ;
#5870=FILL_AREA_STYLE ('',( #6358 ) ) ;
#5900=DIRECTION ( 'NONE',  ( -1.734723475976806848E-16, 1.000000000000000000, 0.000000000000000000 ) ) ;
#5909=ORIENTED_EDGE ( 'NONE', *, *, #2435, .T. ) ;
#5918=UNCERTAINTY_MEASURE_WITH_UNIT (LENGTH_MEASURE( 1.000000000000000082E-05 ), #665, 'distance_accuracy_value', 'NONE');
#5922=DIRECTION ( 'NONE',  ( -1.000000000000000000, 0.000000000000000000, 0.000000000000000000 ) ) ;
#5925=FACE_OUTER_BOUND ( 'NONE', #614, .T. ) ;
#5976=DIRECTION ( 'NONE',  ( 1.000000000000000000, -1.734723475976806848E-16, 0.000000000000000000 ) ) ;
#5994=ADVANCED_FACE ( 'NONE', ( #7863 ), #7293, .F. ) ;
#5996=ORIENTED_EDGE ( 'NONE', *, *, #8392, .T. ) ;
#6033=CARTESIAN_POINT ( 'NONE',  ( 10.00000000000000000, 0.000000000000000000, -63.99999999999997158 ) ) ;
#6039=( NAMED_UNIT ( * ) SI_UNIT ( $, .STERADIAN. ) SOLID_ANGLE_UNIT ( ) );
#6056=DIRECTION ( 'NONE',  ( 0.000000000000000000, -1.000000000000000000, 0.000000000000000000 ) ) ;
#6069=PLANE ( 'NONE',  #3706 ) ;
#6071=VERTEX_POINT ( 'NONE', #8481 ) ;
#6076=ADVANCED_FACE ( 'NONE', ( #5845 ), #4634, .F. ) ;
#6090=CIRCLE ( 'NONE', #4851, 20.00000000000000000 ) ;
#6101=VERTEX_POINT ( 'NONE', #6633 ) ;
#6113=ORIENTED_EDGE ( 'NONE', *, *, #2435, .F. ) ;
#6125=DIRECTION ( 'NONE',  ( -0.000000000000000000, -0.000000000000000000, 1.000000000000000000 ) ) ;
#6203=ORIENTED_EDGE ( 'NONE', *, *, #3534, .T. ) ;
#6223=CARTESIAN_POINT ( 'NONE',  ( -10.00000000000000000, 1.224646799147353256E-15, -63.99999999999997158 ) ) ;
#6239=EDGE_CURVE ( 'NONE', #243, #5734, #5413, .T. ) ;
#6254=ADVANCED_BREP_SHAPE_REPRESENTATION ( '', ( #2244, #594 ), #6685 ) ;
#6262=VERTEX_POINT ( 'NONE', #8172 ) ;
#6280=ORIENTED_EDGE ( 'NONE', *, *, #7991, .F. ) ;
#6311=VECTOR ( 'NONE', #6125, 1000.000000000000000 ) ;
#6320=DIRECTION ( 'NONE',  ( -1.000000000000000000, 0.000000000000000000, -0.000000000000000000 ) ) ;
#6321=DIRECTION ( 'NONE',  ( -0.000000000000000000, -0.000000000000000000, 1.000000000000000000 ) ) ;
#6324=ORIENTED_EDGE ( 'NONE', *, *, #8567, .T. ) ;
#6340=CARTESIAN_POINT ( 'NONE',  ( -5.000000000000000000, -5.000000000000000000, -63.99999999999997158 ) ) ;
#6358=FILL_AREA_STYLE_COLOUR ( '', #2246 ) ;
#6364=LINE ( 'NONE', #1851, #1243 ) ;
#6382=ORIENTED_EDGE ( 'NONE', *, *, #7315, .T. ) ;
#6390=EDGE_LOOP ( 'NONE', ( #4165, #3969, #1175, #3826 ) ) ;
#6408=EDGE_CURVE ( 'NONE', #3015, #6071, #5631, .T. ) ;
#6410=STYLED_ITEM ( 'NONE', ( #2659 ), #6254 ) ;
#6428=DIRECTION ( 'NONE',  ( -0.000000000000000000, -0.000000000000000000, 1.000000000000000000 ) ) ;
#6436=DIRECTION ( 'NONE',  ( -1.000000000000000000, 0.000000000000000000, -0.000000000000000000 ) ) ;
#6442=DIRECTION ( 'NONE',  ( -0.000000000000000000, -0.000000000000000000, 1.000000000000000000 ) ) ;
#6470=VECTOR ( 'NONE', #5773, 1000.000000000000000 ) ;
#6471=LINE ( 'NONE', #6340, #6470 ) ;
#6504=ORIENTED_EDGE ( 'NONE', *, *, #4741, .T. ) ;
#6517=CARTESIAN_POINT ( 'NONE',  ( 0.000000000000000000, 0.000000000000000000, 120.0000000000000142 ) ) ;
#6537=ADVANCED_FACE ( 'NONE', ( #1154 ), #8474, .F. ) ;
#6546=DIRECTION ( 'NONE',  ( 0.000000000000000000, -0.000000000000000000, 1.000000000000000000 ) ) ;
#6549=ORIENTED_EDGE ( 'NONE', *, *, #3300, .F. ) ;
#6560=AXIS2_PLACEMENT_3D ( 'NONE', #842, #5444, #2150 ) ;
#6569=LINE ( 'NONE', #3972, #2270 ) ;
#6574=VERTEX_POINT ( 'NONE', #4577 ) ;
#6584=DIRECTION ( 'NONE',  ( 1.000000000000000000, 0.000000000000000000, -0.000000000000000000 ) ) ;
#6597=PRODUCT_CONTEXT ( 'NONE', #351, 'mechanical' ) ;
#6633=CARTESIAN_POINT ( 'NONE',  ( -20.00000000000000000, 2.449293598294706513E-15, 120.0000000000000142 ) ) ;
#6635=EDGE_CURVE ( 'NONE', #3690, #989, #3574, .T. ) ;
#6642=CYLINDRICAL_SURFACE ( 'NONE', #5033, 20.00000000000000000 ) ;
#6658=ORIENTED_EDGE ( 'NONE', *, *, #6886, .T. ) ;
#6659=DIRECTION ( 'NONE',  ( 1.000000000000000000, 0.000000000000000000, 0.000000000000000000 ) ) ;
#6675=EDGE_LOOP ( 'NONE', ( #2494, #684 ) ) ;
#6685=( GEOMETRIC_REPRESENTATION_CONTEXT ( 3 ) GLOBAL_UNCERTAINTY_ASSIGNED_CONTEXT ( ( #5759 ) ) GLOBAL_UNIT_ASSIGNED_CONTEXT ( ( #349, #8373, #5661 ) ) REPRESENTATION_CONTEXT ( 'NONE', 'WORKASPACE' ) );
#6708=PLANE ( 'NONE',  #2376 ) ;
#6749=CARTESIAN_POINT ( 'NONE',  ( -5.000000000000000000, -5.000000000000000000, 148.0000000000000284 ) ) ;
#6757=CARTESIAN_POINT ( 'NONE',  ( -20.00000000000000000, 2.449293598294706513E-15, -120.5685424949237898 ) ) ;
#6786=ORIENTED_EDGE ( 'NONE', *, *, #5181, .T. ) ;
#6791=ORIENTED_EDGE ( 'NONE', *, *, #2271, .T. ) ;
#6796=EDGE_CURVE ( 'NONE', #5505, #479, #7051, .T. ) ;
#6798=CARTESIAN_POINT ( 'NONE',  ( 0.000000000000000000, 0.000000000000000000, -63.99999999999997158 ) ) ;
#6810=CARTESIAN_POINT ( 'NONE',  ( -5.000000000000000000, -5.000000000000000000, 148.0000000000000284 ) ) ;
#6817=EDGE_LOOP ( 'NONE', ( #8576, #4095 ) ) ;
#6835=ADVANCED_FACE ( 'NONE', ( #4518 ), #3055, .T. ) ;
#6863=EDGE_LOOP ( 'NONE', ( #2985, #8347 ) ) ;
#6871=ORIENTED_EDGE ( 'NONE', *, *, #3689, .T. ) ;
#6877=AXIS2_PLACEMENT_3D ( 'NONE', #7999, #2682, #5976 ) ;
#6886=EDGE_CURVE ( 'NONE', #7751, #4379, #7423, .T. ) ;
#6904=( GEOMETRIC_REPRESENTATION_CONTEXT ( 3 ) GLOBAL_UNCERTAINTY_ASSIGNED_CONTEXT ( ( #5918 ) ) GLOBAL_UNIT_ASSIGNED_CONTEXT ( ( #665, #2787, #5431 ) ) REPRESENTATION_CONTEXT ( 'NONE', 'WORKASPACE' ) );
#6919=EDGE_CURVE ( 'NONE', #7567, #2207, #5295, .T. ) ;
#6937=VECTOR ( 'NONE', #5010, 1000.000000000000000 ) ;
#6941=CARTESIAN_POINT ( 'NONE',  ( 20.00000000000000000, 0.000000000000000000, 120.0000000000000142 ) ) ;
#6952=DIRECTION ( 'NONE',  ( -1.000000000000000000, 0.000000000000000000, 0.000000000000000000 ) ) ;
#7007=AXIS2_PLACEMENT_3D ( 'NONE', #7671, #6442, #3703 ) ;
#7019=CARTESIAN_POINT ( 'NONE',  ( 0.000000000000000000, 0.000000000000000000, -63.99999999999997158 ) ) ;
#7051=LINE ( 'NONE', #4400, #7154 ) ;
#7059=DIRECTION ( 'NONE',  ( -1.000000000000000000, 0.000000000000000000, 0.000000000000000000 ) ) ;
#7061=CARTESIAN_POINT ( 'NONE',  ( 5.000000000000000000, -5.000000000000000000, 148.0000000000000284 ) ) ;
#7078=ORIENTED_EDGE ( 'NONE', *, *, #3832, .T. ) ;
#7117=CARTESIAN_POINT ( 'NONE',  ( 5.000000000000000000, 5.000000000000000000, -63.99999999999997158 ) ) ;
#7129=AXIS2_PLACEMENT_3D ( 'NONE', #3876, #2612, #3915 ) ;
#7141=FACE_OUTER_BOUND ( 'NONE', #5453, .T. ) ;
#7154=VECTOR ( 'NONE', #7717, 1000.000000000000000 ) ;
#7176=CIRCLE ( 'NONE', #1065, 10.00000000000000000 ) ;
#7177=EDGE_CURVE ( 'NONE', #3488, #1501, #5557, .T. ) ;
#7189=CARTESIAN_POINT ( 'NONE',  ( 0.000000000000000000, 0.000000000000000000, -63.99999999999997158 ) ) ;
#7190=CARTESIAN_POINT ( 'NONE',  ( -5.000000000000001776, 5.000000000000001776, 148.0000000000000284 ) ) ;
#7211=CARTESIAN_POINT ( 'NONE',  ( 0.000000000000000000, 0.000000000000000000, -120.5685424949237898 ) ) ;
#7237=ORIENTED_EDGE ( 'NONE', *, *, #1380, .F. ) ;
#7247=CARTESIAN_POINT ( 'NONE',  ( -5.000000000000001776, 5.000000000000001776, 148.0000000000000284 ) ) ;
#7266=SHAPE_REPRESENTATION_RELATIONSHIP ( 'NONE' , 'NONE' ,  #7424, #6254 ) ;
#7267=ORIENTED_EDGE ( 'NONE', *, *, #6919, .T. ) ;
#7291=EDGE_CURVE ( 'NONE', #732, #2207, #1651, .T. ) ;
#7293=PLANE ( 'NONE',  #6877 ) ;
#7294=DIRECTION ( 'NONE',  ( -0.000000000000000000, -0.000000000000000000, 1.000000000000000000 ) ) ;
#7315=EDGE_CURVE ( 'NONE', #6262, #8169, #4341, .T. ) ;
#7348=VERTEX_POINT ( 'NONE', #8357 ) ;
#7363=LINE ( 'NONE', #6749, #7785 ) ;
#7388=( GEOMETRIC_REPRESENTATION_CONTEXT ( 3 ) GLOBAL_UNCERTAINTY_ASSIGNED_CONTEXT ( ( #5066 ) ) GLOBAL_UNIT_ASSIGNED_CONTEXT ( ( #5349, #7884, #6039 ) ) REPRESENTATION_CONTEXT ( 'NONE', 'WORKASPACE' ) );
#7401=AXIS2_PLACEMENT_3D ( 'NONE', #2285, #7540, #8246 ) ;
#7407=EDGE_CURVE ( 'NONE', #1501, #3441, #3252, .T. ) ;
#7410=VECTOR ( 'NONE', #5203, 1000.000000000000000 ) ;
#7423=CIRCLE ( 'NONE', #7007, 20.00000000000000000 ) ;
#7424=SHAPE_REPRESENTATION ( 'roller axis assy_r3', ( #594 ), #6685 ) ;
#7440=EDGE_CURVE ( 'NONE', #1525, #147, #636, .T. ) ;
#7448=ORIENTED_EDGE ( 'NONE', *, *, #5181, .F. ) ;
#7491=VECTOR ( 'NONE', #6056, 1000.000000000000000 ) ;
#7505=EDGE_LOOP ( 'NONE', ( #5170, #4982, #420, #7448 ) ) ;
#7510=CARTESIAN_POINT ( 'NONE',  ( 5.000000000000000000, -5.000000000000000000, -63.99999999999997158 ) ) ;
#7522=CARTESIAN_POINT ( 'NONE',  ( 5.000000000000000000, -5.000000000000000000, 148.0000000000000284 ) ) ;
#7524=EDGE_CURVE ( 'NONE', #6071, #479, #3338, .T. ) ;
#7540=DIRECTION ( 'NONE',  ( 0.000000000000000000, 0.000000000000000000, -1.000000000000000000 ) ) ;
#7547=CARTESIAN_POINT ( 'NONE',  ( 5.000000000000000000, 5.000000000000000000, -71.99999999999998579 ) ) ;
#7549=VERTEX_POINT ( 'NONE', #56 ) ;
#7550=VECTOR ( 'NONE', #7294, 1000.000000000000000 ) ;
#7567=VERTEX_POINT ( 'NONE', #7510 ) ;
#7640=DIRECTION ( 'NONE',  ( -0.000000000000000000, 0.000000000000000000, 1.000000000000000000 ) ) ;
#7671=CARTESIAN_POINT ( 'NONE',  ( 0.000000000000000000, 0.000000000000000000, -43.99999999999997158 ) ) ;
#7676=ORIENTED_EDGE ( 'NONE', *, *, #4886, .T. ) ;
#7690=AXIS2_PLACEMENT_3D ( 'NONE', #2335, #2976, #6320 ) ;
#7715=ORIENTED_EDGE ( 'NONE', *, *, #3689, .F. ) ;
#7717=DIRECTION ( 'NONE',  ( 1.000000000000000000, -1.734723475976806848E-16, 0.000000000000000000 ) ) ;
#7726=CARTESIAN_POINT ( 'NONE',  ( -5.000000000000001776, 5.000000000000001776, 140.0000000000000000 ) ) ;
#7735=DIRECTION ( 'NONE',  ( 1.000000000000000000, -1.734723475976806848E-16, 0.000000000000000000 ) ) ;
#7751=VERTEX_POINT ( 'NONE', #5065 ) ;
#7769=PLANE ( 'NONE',  #1671 ) ;
#7785=VECTOR ( 'NONE', #6659, 1000.000000000000000 ) ;
#7798=AXIS2_PLACEMENT_3D ( 'NONE', #7189, #6321, #1720 ) ;
#7808=DIRECTION ( 'NONE',  ( 0.000000000000000000, 0.000000000000000000, -1.000000000000000000 ) ) ;
#7812=CARTESIAN_POINT ( 'NONE',  ( 5.000000000000000000, -5.000000000000000000, -71.99999999999998579 ) ) ;
#7851=CARTESIAN_POINT ( 'NONE',  ( 0.000000000000000000, 0.000000000000000000, -63.99999999999997158 ) ) ;
#7863=FACE_OUTER_BOUND ( 'NONE', #4155, .T. ) ;
#7872=DIRECTION ( 'NONE',  ( 1.000000000000000000, 0.000000000000000000, 0.000000000000000000 ) ) ;
#7884=( NAMED_UNIT ( * ) PLANE_ANGLE_UNIT ( ) SI_UNIT ( $, .RADIAN. ) );
#7900=CARTESIAN_POINT ( 'NONE',  ( -5.000000000000001776, 5.000000000000001776, -71.99999999999998579 ) ) ;
#7954=VECTOR ( 'NONE', #3811, 1000.000000000000000 ) ;
#7991=EDGE_CURVE ( 'NONE', #1525, #243, #4145, .T. ) ;
#7999=CARTESIAN_POINT ( 'NONE',  ( -5.000000000000001776, 5.000000000000001776, -71.99999999999998579 ) ) ;
#8023=ORIENTED_EDGE ( 'NONE', *, *, #338, .F. ) ;
#8028=LINE ( 'NONE', #2063, #959 ) ;
#8097=FACE_OUTER_BOUND ( 'NONE', #1266, .T. ) ;
#8104=PRODUCT ( 'roller axis assy_r3', 'roller axis assy_r3', '', ( #6597 ) ) ;
#8122=DIRECTION ( 'NONE',  ( -0.000000000000000000, -0.000000000000000000, -1.000000000000000000 ) ) ;
#8128=ORIENTED_EDGE ( 'NONE', *, *, #6796, .T. ) ;
#8129=EDGE_CURVE ( 'NONE', #3441, #243, #4236, .T. ) ;
#8151=ORIENTED_EDGE ( 'NONE', *, *, #3282, .T. ) ;
#8163=DIRECTION ( 'NONE',  ( -0.000000000000000000, -0.000000000000000000, 1.000000000000000000 ) ) ;
#8169=VERTEX_POINT ( 'NONE', #973 ) ;
#8172=CARTESIAN_POINT ( 'NONE',  ( -10.00000000000000000, 1.224646799147353256E-15, -63.99999999999997158 ) ) ;
#8173=ADVANCED_FACE ( 'NONE', ( #5573 ), #8295, .T. ) ;
#8214=ORIENTED_EDGE ( 'NONE', *, *, #525, .F. ) ;
#8246=DIRECTION ( 'NONE',  ( -1.000000000000000000, 0.000000000000000000, 0.000000000000000000 ) ) ;
#8266=ORIENTED_EDGE ( 'NONE', *, *, #7291, .F. ) ;
#8269=LINE ( 'NONE', #2307, #7954 ) ;
#8278=DIRECTION ( 'NONE',  ( 0.000000000000000000, 0.000000000000000000, -1.000000000000000000 ) ) ;
#8295=PLANE ( 'NONE',  #7690 ) ;
#8297=FACE_OUTER_BOUND ( 'NONE', #4821, .T. ) ;
#8322=DIRECTION ( 'NONE',  ( 0.000000000000000000, 0.000000000000000000, -1.000000000000000000 ) ) ;
#8333=EDGE_LOOP ( 'NONE', ( #1966, #4485, #7078, #2780 ) ) ;
#8347=ORIENTED_EDGE ( 'NONE', *, *, #4994, .F. ) ;
#8357=CARTESIAN_POINT ( 'NONE',  ( 5.000000000000000000, -5.000000000000000000, -71.99999999999998579 ) ) ;
#8373=( NAMED_UNIT ( * ) PLANE_ANGLE_UNIT ( ) SI_UNIT ( $, .RADIAN. ) );
#8392=EDGE_CURVE ( 'NONE', #5734, #1501, #17, .T. ) ;
#8397=VECTOR ( 'NONE', #3555, 1000.000000000000000 ) ;
#8450=ORIENTED_EDGE ( 'NONE', *, *, #8392, .F. ) ;
#8468=FACE_OUTER_BOUND ( 'NONE', #5418, .T. ) ;
#8474=PLANE ( 'NONE',  #2292 ) ;
#8481=CARTESIAN_POINT ( 'NONE',  ( 5.000000000000000000, 5.000000000000000000, -71.99999999999998579 ) ) ;
#8490=FACE_OUTER_BOUND ( 'NONE', #7505, .T. ) ;
#8518=CARTESIAN_POINT ( 'NONE',  ( 5.000000000000000000, -5.000000000000000000, -71.99999999999998579 ) ) ;
#8519=CIRCLE ( 'NONE', #7401, 10.00000000000000000 ) ;
#8531=ORIENTED_EDGE ( 'NONE', *, *, #4704, .T. ) ;
#8541=VERTEX_POINT ( 'NONE', #2815 ) ;
#8544=SURFACE_STYLE_USAGE ( .BOTH. , #3229 ) ;
#8567=EDGE_CURVE ( 'NONE', #7348, #732, #4817, .T. ) ;
#8576=ORIENTED_EDGE ( 'NONE', *, *, #5409, .T. ) ;
#8582=AXIS2_PLACEMENT_3D ( 'NONE', #4462, #3124, #543 ) ;
#8586=SURFACE_STYLE_FILL_AREA ( #5870 ) ;
#8672=COLOUR_RGB('Off White',0.89,0.88,0.83);
#8673=FILL_AREA_STYLE_COLOUR('',#8672);
#8674=FILL_AREA_STYLE('',(#8673));
#8675=SURFACE_STYLE_FILL_AREA(#8674);
#8676=SURFACE_SIDE_STYLE('',(#8675));
#8677=SURFACE_STYLE_USAGE(.BOTH.,#8676);
#8678=PRESENTATION_STYLE_ASSIGNMENT((#8677));
ENDSEC;
END-ISO-10303-21;
